ISO-10303-21;
HEADER;
/* Generated by software containing ST-Developer
 * from STEP Tools, Inc. (www.steptools.com) 
 */

FILE_DESCRIPTION(
/* description */ ('Shaft runout checking stand'),
/* implementation_level */ '2;1');

FILE_NAME(
/* name */ 'Inner race spacer (2).step',
/* time_stamp */ '2026-11-02T21:12:33-08:00',
/* author */ (''),
/* organization */ (''),
/* preprocessor_version */ 'ST-DEVELOPER v20.2',
/* originating_system */ 'Autodesk Translation Framework v15.17.0.0',
/* authorisation */ '');

FILE_SCHEMA (('AUTOMOTIVE_DESIGN { 1 0 10303 214 3 1 1 }'));
ENDSEC;

DATA;
#10=MECHANICAL_DESIGN_GEOMETRIC_PRESENTATION_REPRESENTATION('',(#494),#11748);
#408=SHAPE_REPRESENTATION_RELATIONSHIP('SRR','None',#11957,#451);
#451=ADVANCED_BREP_SHAPE_REPRESENTATION('',(#542),#11733);
#494=STYLED_ITEM('',(#12170),#542);
#542=MANIFOLD_SOLID_BREP('Body1',#6240);
#652=FACE_BOUND('',#1789,.T.);
#653=FACE_BOUND('',#1791,.T.);
#840=CIRCLE('',#7228,0.505);
#841=CIRCLE('',#7229,0.505);
#842=CIRCLE('',#7231,0.7);
#843=CIRCLE('',#7232,0.7);
#1013=CYLINDRICAL_SURFACE('',#7227,0.505);
#1014=CYLINDRICAL_SURFACE('',#7230,0.7);
#1328=FACE_OUTER_BOUND('',#1786,.T.);
#1329=FACE_OUTER_BOUND('',#1787,.T.);
#1330=FACE_OUTER_BOUND('',#1788,.T.);
#1331=FACE_OUTER_BOUND('',#1790,.T.);
#1786=EDGE_LOOP('',(#5314,#5315,#5316,#5317));
#1787=EDGE_LOOP('',(#5318,#5319,#5320,#5321));
#1788=EDGE_LOOP('',(#5322));
#1789=EDGE_LOOP('',(#5323));
#1790=EDGE_LOOP('',(#5324));
#1791=EDGE_LOOP('',(#5325));
#2323=LINE('',#10899,#2790);
#2324=LINE('',#10905,#2791);
#2790=VECTOR('',#8920,0.505);
#2791=VECTOR('',#8927,0.7);
#3224=VERTEX_POINT('',#10896);
#3225=VERTEX_POINT('',#10898);
#3226=VERTEX_POINT('',#10902);
#3227=VERTEX_POINT('',#10904);
#3943=EDGE_CURVE('',#3224,#3224,#840,.T.);
#3944=EDGE_CURVE('',#3224,#3225,#2323,.T.);
#3945=EDGE_CURVE('',#3225,#3225,#841,.T.);
#3946=EDGE_CURVE('',#3226,#3226,#842,.T.);
#3947=EDGE_CURVE('',#3226,#3227,#2324,.T.);
#3948=EDGE_CURVE('',#3227,#3227,#843,.T.);
#5314=ORIENTED_EDGE('',*,*,#3943,.F.);
#5315=ORIENTED_EDGE('',*,*,#3944,.T.);
#5316=ORIENTED_EDGE('',*,*,#3945,.T.);
#5317=ORIENTED_EDGE('',*,*,#3944,.F.);
#5318=ORIENTED_EDGE('',*,*,#3946,.F.);
#5319=ORIENTED_EDGE('',*,*,#3947,.T.);
#5320=ORIENTED_EDGE('',*,*,#3948,.T.);
#5321=ORIENTED_EDGE('',*,*,#3947,.F.);
#5322=ORIENTED_EDGE('',*,*,#3946,.T.);
#5323=ORIENTED_EDGE('',*,*,#3943,.T.);
#5324=ORIENTED_EDGE('',*,*,#3948,.F.);
#5325=ORIENTED_EDGE('',*,*,#3945,.F.);
#5807=PLANE('',#7233);
#5808=PLANE('',#7234);
#6128=ADVANCED_FACE('',(#1328),#1013,.F.);
#6129=ADVANCED_FACE('',(#1329),#1014,.T.);
#6130=ADVANCED_FACE('',(#1330,#652),#5807,.T.);
#6131=ADVANCED_FACE('',(#1331,#653),#5808,.F.);
#6240=CLOSED_SHELL('',(#6128,#6129,#6130,#6131));
#7226=AXIS2_PLACEMENT_3D('',#10894,#8914,#8915);
#7227=AXIS2_PLACEMENT_3D('',#10895,#8916,#8917);
#7228=AXIS2_PLACEMENT_3D('',#10897,#8918,#8919);
#7229=AXIS2_PLACEMENT_3D('',#10900,#8921,#8922);
#7230=AXIS2_PLACEMENT_3D('',#10901,#8923,#8924);
#7231=AXIS2_PLACEMENT_3D('',#10903,#8925,#8926);
#7232=AXIS2_PLACEMENT_3D('',#10906,#8928,#8929);
#7233=AXIS2_PLACEMENT_3D('',#10907,#8930,#8931);
#7234=AXIS2_PLACEMENT_3D('',#10908,#8932,#8933);
#8914=DIRECTION('axis',(0.,0.,1.));
#8915=DIRECTION('refdir',(1.,0.,0.));
#8916=DIRECTION('center_axis',(0.,1.,0.));
#8917=DIRECTION('ref_axis',(1.,0.,0.));
#8918=DIRECTION('center_axis',(0.,-1.,0.));
#8919=DIRECTION('ref_axis',(1.,0.,0.));
#8920=DIRECTION('',(0.,-1.,0.));
#8921=DIRECTION('center_axis',(0.,-1.,0.));
#8922=DIRECTION('ref_axis',(1.,0.,0.));
#8923=DIRECTION('center_axis',(0.,1.,0.));
#8924=DIRECTION('ref_axis',(1.,0.,0.));
#8925=DIRECTION('center_axis',(0.,1.,0.));
#8926=DIRECTION('ref_axis',(1.,0.,0.));
#8927=DIRECTION('',(0.,-1.,0.));
#8928=DIRECTION('center_axis',(0.,1.,0.));
#8929=DIRECTION('ref_axis',(1.,0.,0.));
#8930=DIRECTION('center_axis',(0.,1.,0.));
#8931=DIRECTION('ref_axis',(1.,0.,0.));
#8932=DIRECTION('center_axis',(0.,1.,0.));
#8933=DIRECTION('ref_axis',(1.,0.,0.));
#10894=CARTESIAN_POINT('',(0.,0.,0.));
#10895=CARTESIAN_POINT('Origin',(2.,-10.8,5.));
#10896=CARTESIAN_POINT('',(1.495,-10.45,5.));
#10897=CARTESIAN_POINT('Origin',(2.,-10.45,5.));
#10898=CARTESIAN_POINT('',(1.495,-10.8,5.));
#10899=CARTESIAN_POINT('',(1.495,-10.8,5.));
#10900=CARTESIAN_POINT('Origin',(2.,-10.8,5.));
#10901=CARTESIAN_POINT('Origin',(2.,-10.8,5.));
#10902=CARTESIAN_POINT('',(1.3,-10.45,5.));
#10903=CARTESIAN_POINT('Origin',(2.,-10.45,5.));
#10904=CARTESIAN_POINT('',(1.3,-10.8,5.));
#10905=CARTESIAN_POINT('',(1.3,-10.8,5.));
#10906=CARTESIAN_POINT('Origin',(2.,-10.8,5.));
#10907=CARTESIAN_POINT('Origin',(2.,-10.45,5.));
#10908=CARTESIAN_POINT('Origin',(2.,-10.8,5.));
#11684=UNCERTAINTY_MEASURE_WITH_UNIT(LENGTH_MEASURE(0.001),#11749,
'DISTANCE_ACCURACY_VALUE',
'Maximum model space distance between geometric entities at asserted c
onnectivities');
#11699=UNCERTAINTY_MEASURE_WITH_UNIT(LENGTH_MEASURE(0.001),#11749,
'DISTANCE_ACCURACY_VALUE',
'Maximum model space distance between geometric entities at asserted c
onnectivities');
#11733=(
GEOMETRIC_REPRESENTATION_CONTEXT(3)
GLOBAL_UNCERTAINTY_ASSIGNED_CONTEXT((#11684))
GLOBAL_UNIT_ASSIGNED_CONTEXT((#11749,#11751,#11752))
REPRESENTATION_CONTEXT('','3D')
);
#11748=(
GEOMETRIC_REPRESENTATION_CONTEXT(3)
GLOBAL_UNCERTAINTY_ASSIGNED_CONTEXT((#11699))
GLOBAL_UNIT_ASSIGNED_CONTEXT((#11749,#11751,#11752))
REPRESENTATION_CONTEXT('','3D')
);
#11749=(
LENGTH_UNIT()
NAMED_UNIT(*)
SI_UNIT(.CENTI.,.METRE.)
);
#11751=(
NAMED_UNIT(*)
PLANE_ANGLE_UNIT()
SI_UNIT($,.RADIAN.)
);
#11752=(
NAMED_UNIT(*)
SI_UNIT($,.STERADIAN.)
SOLID_ANGLE_UNIT()
);
#11786=SHAPE_DEFINITION_REPRESENTATION(#11834,#11957);
#11834=PRODUCT_DEFINITION_SHAPE('',$,#12006);
#11957=SHAPE_REPRESENTATION('',(#7226),#11733);
#11972=PRODUCT_DEFINITION_CONTEXT('part definition',#12118,'design');
#12006=PRODUCT_DEFINITION('Inner race spacer_5','Inner race spacer (2)',
#12054,#11972);
#12054=PRODUCT_DEFINITION_FORMATION('',$,#12153);
#12118=APPLICATION_CONTEXT(
'Core Data for Automotive Mechanical Design Process');
#12119=PRODUCT_CONTEXT('part definition',#12118,'mechanical');
#12153=PRODUCT('Inner race spacer_5','Inner race spacer (2)',
'Inner race spacer',(#12119));
#12170=PRESENTATION_STYLE_ASSIGNMENT((#12175));
#12175=SURFACE_STYLE_USAGE(.BOTH.,#12180);
#12180=SURFACE_SIDE_STYLE('',(#12185));
#12185=SURFACE_STYLE_FILL_AREA(#12190);
#12190=FILL_AREA_STYLE('CAD Library Painted - Steel gray',(#12195));
#12195=FILL_AREA_STYLE_COLOUR('CAD Library Painted - Steel gray',#12200);
#12200=COLOUR_RGB('CAD Library Painted - Steel gray',0.592156862745098,
0.631372549019608,0.67843137254902);
ENDSEC;
END-ISO-10303-21;
